ISO-10303-21;
HEADER;
/* Generated by software containing ST-Developer
 * from STEP Tools, Inc. (www.steptools.com) 
 */

FILE_DESCRIPTION(
/* description */ (''),
/* implementation_level */ '2;1');

FILE_NAME(
/* name */ 'Bearing_01.step',
/* time_stamp */ '2026-10-19T01:30:23+06:00',
/* author */ (''),
/* organization */ (''),
/* preprocessor_version */ 'ST-DEVELOPER v20.2',
/* originating_system */ 'Autodesk Translation Framework v15.15.0.0',
/* authorisation */ '');

FILE_SCHEMA (('AUTOMOTIVE_DESIGN { 1 0 10303 214 3 1 1 }'));
ENDSEC;

DATA;
#10=MECHANICAL_DESIGN_GEOMETRIC_PRESENTATION_REPRESENTATION('',(#95),#10639);
#75=SHAPE_REPRESENTATION_RELATIONSHIP('SRR','None',#10685,#85);
#85=ADVANCED_BREP_SHAPE_REPRESENTATION('',(#105),#10637);
#95=STYLED_ITEM('',(#10790),#105);
#105=MANIFOLD_SOLID_BREP('Bearing_01',#5721);
#231=TOROIDAL_SURFACE('',#6465,4.3,0.3);
#232=TOROIDAL_SURFACE('',#6475,4.7,0.3);
#233=TOROIDAL_SURFACE('',#6482,4.3,0.3);
#234=TOROIDAL_SURFACE('',#6487,4.7,0.3);
#284=FACE_BOUND('',#1094,.T.);
#285=FACE_BOUND('',#1100,.T.);
#365=PLANE('',#6470);
#366=PLANE('',#6485);
#668=FACE_OUTER_BOUND('',#1092,.T.);
#669=FACE_OUTER_BOUND('',#1093,.T.);
#670=FACE_OUTER_BOUND('',#1095,.T.);
#671=FACE_OUTER_BOUND('',#1096,.T.);
#672=FACE_OUTER_BOUND('',#1097,.T.);
#673=FACE_OUTER_BOUND('',#1098,.T.);
#674=FACE_OUTER_BOUND('',#1099,.T.);
#675=FACE_OUTER_BOUND('',#1101,.T.);
#1092=EDGE_LOOP('',(#4720,#4721,#4722,#4723,#4724));
#1093=EDGE_LOOP('',(#4725));
#1094=EDGE_LOOP('',(#4726));
#1095=EDGE_LOOP('',(#4727,#4728,#4729,#4730,#4731,#4732));
#1096=EDGE_LOOP('',(#4733,#4734,#4735,#4736,#4737));
#1097=EDGE_LOOP('',(#4738,#4739,#4740,#4741,#4742,#4743));
#1098=EDGE_LOOP('',(#4744,#4745,#4746,#4747,#4748));
#1099=EDGE_LOOP('',(#4749));
#1100=EDGE_LOOP('',(#4750));
#1101=EDGE_LOOP('',(#4751,#4752,#4753,#4754,#4755));
#1444=LINE('',#10078,#1774);
#1445=LINE('',#10090,#1775);
#1774=VECTOR('',#8214,4.);
#1775=VECTOR('',#8229,5.);
#2184=CIRCLE('',#6466,4.3);
#2185=CIRCLE('',#6467,0.3);
#2186=CIRCLE('',#6468,4.);
#2187=CIRCLE('',#6469,4.);
#2188=CIRCLE('',#6471,4.7);
#2189=CIRCLE('',#6473,4.);
#2190=CIRCLE('',#6474,4.);
#2191=CIRCLE('',#6476,0.3);
#2192=CIRCLE('',#6477,5.);
#2193=CIRCLE('',#6478,5.);
#2194=CIRCLE('',#6480,5.);
#2195=CIRCLE('',#6481,5.);
#2196=CIRCLE('',#6483,4.3);
#2197=CIRCLE('',#6484,0.3);
#2198=CIRCLE('',#6486,4.7);
#2199=CIRCLE('',#6488,0.3);
#2634=VERTEX_POINT('',#10066);
#2635=VERTEX_POINT('',#10068);
#2636=VERTEX_POINT('',#10070);
#2637=VERTEX_POINT('',#10074);
#2638=VERTEX_POINT('',#10077);
#2639=VERTEX_POINT('',#10079);
#2640=VERTEX_POINT('',#10083);
#2641=VERTEX_POINT('',#10085);
#2642=VERTEX_POINT('',#10089);
#2643=VERTEX_POINT('',#10091);
#2644=VERTEX_POINT('',#10095);
#2645=VERTEX_POINT('',#10099);
#3336=EDGE_CURVE('',#2634,#2634,#2184,.T.);
#3337=EDGE_CURVE('',#2634,#2635,#2185,.T.);
#3338=EDGE_CURVE('',#2635,#2636,#2186,.T.);
#3339=EDGE_CURVE('',#2636,#2635,#2187,.T.);
#3340=EDGE_CURVE('',#2637,#2637,#2188,.T.);
#3341=EDGE_CURVE('',#2636,#2638,#1444,.T.);
#3342=EDGE_CURVE('',#2639,#2638,#2189,.T.);
#3343=EDGE_CURVE('',#2638,#2639,#2190,.T.);
#3344=EDGE_CURVE('',#2637,#2640,#2191,.T.);
#3345=EDGE_CURVE('',#2640,#2641,#2192,.T.);
#3346=EDGE_CURVE('',#2641,#2640,#2193,.T.);
#3347=EDGE_CURVE('',#2641,#2642,#1445,.T.);
#3348=EDGE_CURVE('',#2643,#2642,#2194,.T.);
#3349=EDGE_CURVE('',#2642,#2643,#2195,.T.);
#3350=EDGE_CURVE('',#2644,#2644,#2196,.T.);
#3351=EDGE_CURVE('',#2644,#2639,#2197,.T.);
#3352=EDGE_CURVE('',#2645,#2645,#2198,.T.);
#3353=EDGE_CURVE('',#2645,#2643,#2199,.T.);
#4720=ORIENTED_EDGE('',*,*,#3336,.T.);
#4721=ORIENTED_EDGE('',*,*,#3337,.T.);
#4722=ORIENTED_EDGE('',*,*,#3338,.T.);
#4723=ORIENTED_EDGE('',*,*,#3339,.T.);
#4724=ORIENTED_EDGE('',*,*,#3337,.F.);
#4725=ORIENTED_EDGE('',*,*,#3340,.F.);
#4726=ORIENTED_EDGE('',*,*,#3336,.F.);
#4727=ORIENTED_EDGE('',*,*,#3339,.F.);
#4728=ORIENTED_EDGE('',*,*,#3341,.T.);
#4729=ORIENTED_EDGE('',*,*,#3342,.F.);
#4730=ORIENTED_EDGE('',*,*,#3343,.F.);
#4731=ORIENTED_EDGE('',*,*,#3341,.F.);
#4732=ORIENTED_EDGE('',*,*,#3338,.F.);
#4733=ORIENTED_EDGE('',*,*,#3340,.T.);
#4734=ORIENTED_EDGE('',*,*,#3344,.T.);
#4735=ORIENTED_EDGE('',*,*,#3345,.T.);
#4736=ORIENTED_EDGE('',*,*,#3346,.T.);
#4737=ORIENTED_EDGE('',*,*,#3344,.F.);
#4738=ORIENTED_EDGE('',*,*,#3346,.F.);
#4739=ORIENTED_EDGE('',*,*,#3347,.T.);
#4740=ORIENTED_EDGE('',*,*,#3348,.F.);
#4741=ORIENTED_EDGE('',*,*,#3349,.F.);
#4742=ORIENTED_EDGE('',*,*,#3347,.F.);
#4743=ORIENTED_EDGE('',*,*,#3345,.F.);
#4744=ORIENTED_EDGE('',*,*,#3350,.T.);
#4745=ORIENTED_EDGE('',*,*,#3351,.T.);
#4746=ORIENTED_EDGE('',*,*,#3342,.T.);
#4747=ORIENTED_EDGE('',*,*,#3343,.T.);
#4748=ORIENTED_EDGE('',*,*,#3351,.F.);
#4749=ORIENTED_EDGE('',*,*,#3352,.F.);
#4750=ORIENTED_EDGE('',*,*,#3350,.F.);
#4751=ORIENTED_EDGE('',*,*,#3352,.T.);
#4752=ORIENTED_EDGE('',*,*,#3353,.T.);
#4753=ORIENTED_EDGE('',*,*,#3348,.T.);
#4754=ORIENTED_EDGE('',*,*,#3349,.T.);
#4755=ORIENTED_EDGE('',*,*,#3353,.F.);
#5278=CYLINDRICAL_SURFACE('',#6472,4.);
#5279=CYLINDRICAL_SURFACE('',#6479,5.);
#5611=ADVANCED_FACE('',(#668),#231,.T.);
#5612=ADVANCED_FACE('',(#669,#284),#365,.F.);
#5613=ADVANCED_FACE('',(#670),#5278,.F.);
#5614=ADVANCED_FACE('',(#671),#232,.T.);
#5615=ADVANCED_FACE('',(#672),#5279,.T.);
#5616=ADVANCED_FACE('',(#673),#233,.T.);
#5617=ADVANCED_FACE('',(#674,#285),#366,.T.);
#5618=ADVANCED_FACE('',(#675),#234,.T.);
#5721=CLOSED_SHELL('',(#5611,#5612,#5613,#5614,#5615,#5616,#5617,#5618));
#6464=AXIS2_PLACEMENT_3D('',#10064,#8196,#8197);
#6465=AXIS2_PLACEMENT_3D('',#10065,#8198,#8199);
#6466=AXIS2_PLACEMENT_3D('',#10067,#8200,#8201);
#6467=AXIS2_PLACEMENT_3D('',#10069,#8202,#8203);
#6468=AXIS2_PLACEMENT_3D('',#10071,#8204,#8205);
#6469=AXIS2_PLACEMENT_3D('',#10072,#8206,#8207);
#6470=AXIS2_PLACEMENT_3D('',#10073,#8208,#8209);
#6471=AXIS2_PLACEMENT_3D('',#10075,#8210,#8211);
#6472=AXIS2_PLACEMENT_3D('',#10076,#8212,#8213);
#6473=AXIS2_PLACEMENT_3D('',#10080,#8215,#8216);
#6474=AXIS2_PLACEMENT_3D('',#10081,#8217,#8218);
#6475=AXIS2_PLACEMENT_3D('',#10082,#8219,#8220);
#6476=AXIS2_PLACEMENT_3D('',#10084,#8221,#8222);
#6477=AXIS2_PLACEMENT_3D('',#10086,#8223,#8224);
#6478=AXIS2_PLACEMENT_3D('',#10087,#8225,#8226);
#6479=AXIS2_PLACEMENT_3D('',#10088,#8227,#8228);
#6480=AXIS2_PLACEMENT_3D('',#10092,#8230,#8231);
#6481=AXIS2_PLACEMENT_3D('',#10093,#8232,#8233);
#6482=AXIS2_PLACEMENT_3D('',#10094,#8234,#8235);
#6483=AXIS2_PLACEMENT_3D('',#10096,#8236,#8237);
#6484=AXIS2_PLACEMENT_3D('',#10097,#8238,#8239);
#6485=AXIS2_PLACEMENT_3D('',#10098,#8240,#8241);
#6486=AXIS2_PLACEMENT_3D('',#10100,#8242,#8243);
#6487=AXIS2_PLACEMENT_3D('',#10101,#8244,#8245);
#6488=AXIS2_PLACEMENT_3D('',#10102,#8246,#8247);
#8196=DIRECTION('axis',(0.,0.,1.));
#8197=DIRECTION('refdir',(1.,0.,0.));
#8198=DIRECTION('center_axis',(-1.,0.,0.));
#8199=DIRECTION('ref_axis',(0.,0.,1.));
#8200=DIRECTION('center_axis',(1.,0.,0.));
#8201=DIRECTION('ref_axis',(0.,-1.,0.));
#8202=DIRECTION('center_axis',(0.,-1.,0.));
#8203=DIRECTION('ref_axis',(0.,0.,-1.));
#8204=DIRECTION('center_axis',(-1.,0.,0.));
#8205=DIRECTION('ref_axis',(0.,-1.,0.));
#8206=DIRECTION('center_axis',(-1.,0.,0.));
#8207=DIRECTION('ref_axis',(0.,-1.,0.));
#8208=DIRECTION('center_axis',(-1.,0.,0.));
#8209=DIRECTION('ref_axis',(0.,-1.,0.));
#8210=DIRECTION('center_axis',(-1.,0.,0.));
#8211=DIRECTION('ref_axis',(0.,-1.,0.));
#8212=DIRECTION('center_axis',(1.,0.,0.));
#8213=DIRECTION('ref_axis',(0.,-1.,0.));
#8214=DIRECTION('',(-1.,0.,0.));
#8215=DIRECTION('center_axis',(1.,0.,0.));
#8216=DIRECTION('ref_axis',(0.,-1.,0.));
#8217=DIRECTION('center_axis',(1.,0.,0.));
#8218=DIRECTION('ref_axis',(0.,-1.,0.));
#8219=DIRECTION('center_axis',(1.,0.,0.));
#8220=DIRECTION('ref_axis',(0.,0.,-1.));
#8221=DIRECTION('center_axis',(0.,-1.,0.));
#8222=DIRECTION('ref_axis',(0.,0.,1.));
#8223=DIRECTION('center_axis',(1.,0.,0.));
#8224=DIRECTION('ref_axis',(0.,-1.,0.));
#8225=DIRECTION('center_axis',(1.,0.,0.));
#8226=DIRECTION('ref_axis',(0.,-1.,0.));
#8227=DIRECTION('center_axis',(1.,0.,0.));
#8228=DIRECTION('ref_axis',(0.,-1.,0.));
#8229=DIRECTION('',(-1.,0.,0.));
#8230=DIRECTION('center_axis',(-1.,0.,0.));
#8231=DIRECTION('ref_axis',(0.,-1.,0.));
#8232=DIRECTION('center_axis',(-1.,0.,0.));
#8233=DIRECTION('ref_axis',(0.,-1.,0.));
#8234=DIRECTION('center_axis',(1.,0.,0.));
#8235=DIRECTION('ref_axis',(0.,0.,-1.));
#8236=DIRECTION('center_axis',(-1.,0.,0.));
#8237=DIRECTION('ref_axis',(0.,-1.,0.));
#8238=DIRECTION('center_axis',(0.,-1.,0.));
#8239=DIRECTION('ref_axis',(0.,0.,1.));
#8240=DIRECTION('center_axis',(-1.,0.,0.));
#8241=DIRECTION('ref_axis',(0.,-1.,0.));
#8242=DIRECTION('center_axis',(1.,0.,0.));
#8243=DIRECTION('ref_axis',(0.,-1.,0.));
#8244=DIRECTION('center_axis',(-1.,0.,0.));
#8245=DIRECTION('ref_axis',(0.,0.,1.));
#8246=DIRECTION('center_axis',(0.,-1.,0.));
#8247=DIRECTION('ref_axis',(0.,0.,-1.));
#10064=CARTESIAN_POINT('',(0.,0.,0.));
#10065=CARTESIAN_POINT('Origin',(-13.3,21.9999999999999,-1.92966607280848));
#10066=CARTESIAN_POINT('',(-13.,21.9999999999999,-6.22966607280848));
#10067=CARTESIAN_POINT('Origin',(-13.,21.9999999999999,-1.92966607280848));
#10068=CARTESIAN_POINT('',(-13.3,21.9999999999999,-5.92966607280848));
#10069=CARTESIAN_POINT('Origin',(-13.3,21.9999999999999,-6.22966607280848));
#10070=CARTESIAN_POINT('',(-13.3,25.9999999999999,-1.92966607280848));
#10071=CARTESIAN_POINT('Origin',(-13.3,21.9999999999999,-1.92966607280848));
#10072=CARTESIAN_POINT('Origin',(-13.3,21.9999999999999,-1.92966607280848));
#10073=CARTESIAN_POINT('Origin',(-13.,21.9999999999999,-1.92966607280848));
#10074=CARTESIAN_POINT('',(-13.,21.9999999999999,2.77033392719152));
#10075=CARTESIAN_POINT('Origin',(-13.,21.9999999999999,-1.92966607280848));
#10076=CARTESIAN_POINT('Origin',(-29.,21.9999999999999,-1.92966607280848));
#10077=CARTESIAN_POINT('',(-28.7,25.9999999999999,-1.92966607280848));
#10078=CARTESIAN_POINT('',(-29.,25.9999999999999,-1.92966607280848));
#10079=CARTESIAN_POINT('',(-28.7,21.9999999999999,2.07033392719152));
#10080=CARTESIAN_POINT('Origin',(-28.7,21.9999999999999,-1.92966607280848));
#10081=CARTESIAN_POINT('Origin',(-28.7,21.9999999999999,-1.92966607280848));
#10082=CARTESIAN_POINT('Origin',(-13.3,21.9999999999999,-1.92966607280848));
#10083=CARTESIAN_POINT('',(-13.3,21.9999999999999,3.07033392719152));
#10084=CARTESIAN_POINT('Origin',(-13.3,21.9999999999999,2.77033392719152));
#10085=CARTESIAN_POINT('',(-13.3,26.9999999999999,-1.92966607280848));
#10086=CARTESIAN_POINT('Origin',(-13.3,21.9999999999999,-1.92966607280848));
#10087=CARTESIAN_POINT('Origin',(-13.3,21.9999999999999,-1.92966607280848));
#10088=CARTESIAN_POINT('Origin',(-29.,21.9999999999999,-1.92966607280848));
#10089=CARTESIAN_POINT('',(-28.7,26.9999999999999,-1.92966607280848));
#10090=CARTESIAN_POINT('',(-29.,26.9999999999999,-1.92966607280848));
#10091=CARTESIAN_POINT('',(-28.7,21.9999999999999,-6.92966607280848));
#10092=CARTESIAN_POINT('Origin',(-28.7,21.9999999999999,-1.92966607280848));
#10093=CARTESIAN_POINT('Origin',(-28.7,21.9999999999999,-1.92966607280848));
#10094=CARTESIAN_POINT('Origin',(-28.7,21.9999999999999,-1.92966607280848));
#10095=CARTESIAN_POINT('',(-29.,21.9999999999999,2.37033392719152));
#10096=CARTESIAN_POINT('Origin',(-29.,21.9999999999999,-1.92966607280848));
#10097=CARTESIAN_POINT('Origin',(-28.7,21.9999999999999,2.37033392719152));
#10098=CARTESIAN_POINT('Origin',(-29.,21.9999999999999,-1.92966607280848));
#10099=CARTESIAN_POINT('',(-29.,21.9999999999999,-6.62966607280848));
#10100=CARTESIAN_POINT('Origin',(-29.,21.9999999999999,-1.92966607280848));
#10101=CARTESIAN_POINT('Origin',(-28.7,21.9999999999999,-1.92966607280848));
#10102=CARTESIAN_POINT('Origin',(-28.7,21.9999999999999,-6.62966607280848));
#10625=UNCERTAINTY_MEASURE_WITH_UNIT(LENGTH_MEASURE(0.01),#10640,
'DISTANCE_ACCURACY_VALUE',
'Maximum model space distance between geometric entities at asserted c
onnectivities');
#10627=UNCERTAINTY_MEASURE_WITH_UNIT(LENGTH_MEASURE(0.01),#10640,
'DISTANCE_ACCURACY_VALUE',
'Maximum model space distance between geometric entities at asserted c
onnectivities');
#10637=(
GEOMETRIC_REPRESENTATION_CONTEXT(3)
GLOBAL_UNCERTAINTY_ASSIGNED_CONTEXT((#10625))
GLOBAL_UNIT_ASSIGNED_CONTEXT((#10640,#10642,#10643))
REPRESENTATION_CONTEXT('','3D')
);
#10639=(
GEOMETRIC_REPRESENTATION_CONTEXT(3)
GLOBAL_UNCERTAINTY_ASSIGNED_CONTEXT((#10627))
GLOBAL_UNIT_ASSIGNED_CONTEXT((#10640,#10642,#10643))
REPRESENTATION_CONTEXT('','3D')
);
#10640=(
LENGTH_UNIT()
NAMED_UNIT(*)
SI_UNIT(.MILLI.,.METRE.)
);
#10642=(
NAMED_UNIT(*)
PLANE_ANGLE_UNIT()
SI_UNIT($,.RADIAN.)
);
#10643=(
NAMED_UNIT(*)
SI_UNIT($,.STERADIAN.)
SOLID_ANGLE_UNIT()
);
#10653=SHAPE_DEFINITION_REPRESENTATION(#10664,#10685);
#10664=PRODUCT_DEFINITION_SHAPE('',$,#10697);
#10685=SHAPE_REPRESENTATION('',(#6464),#10637);
#10687=PRODUCT_DEFINITION_CONTEXT('part definition',#10722,'design');
#10697=PRODUCT_DEFINITION('Bearing_01','Bearing_01',#10708,#10687);
#10708=PRODUCT_DEFINITION_FORMATION('',$,#10733);
#10722=APPLICATION_CONTEXT(
'Core Data for Automotive Mechanical Design Process');
#10723=PRODUCT_CONTEXT('part definition',#10722,'mechanical');
#10733=PRODUCT('Bearing_01','Bearing_01',$,(#10723));
#10784=COLOUR_RGB('Grey',0.48,0.52,0.57);
#10785=FILL_AREA_STYLE_COLOUR('',#10784);
#10786=FILL_AREA_STYLE('',(#10785));
#10787=SURFACE_STYLE_FILL_AREA(#10786);
#10788=SURFACE_SIDE_STYLE('',(#10787));
#10789=SURFACE_STYLE_USAGE(.BOTH.,#10788);
#10790=PRESENTATION_STYLE_ASSIGNMENT((#10789));
ENDSEC;
END-ISO-10303-21;
